ISO-10303-21;
HEADER;
/* Generated by software containing ST-Developer
 * from STEP Tools, Inc. (www.steptools.com) 
 */

FILE_DESCRIPTION(
/* description */ ('PAT-041'),
/* implementation_level */ '2;1');

FILE_NAME(
/* name */ 'Pipe spool.step',
/* time_stamp */ '2026-10-28T22:21:24-07:00',
/* author */ (''),
/* organization */ (''),
/* preprocessor_version */ 'ST-DEVELOPER v20.2',
/* originating_system */ 'Autodesk Translation Framework v15.17.0.0',
/* authorisation */ '');

FILE_SCHEMA (('AUTOMOTIVE_DESIGN { 1 0 10303 214 3 1 1 }'));
ENDSEC;

DATA;
#10=MECHANICAL_DESIGN_GEOMETRIC_PRESENTATION_REPRESENTATION('',(#209),#2507);
#189=SHAPE_REPRESENTATION_RELATIONSHIP('SRR','None',#2574,#199);
#199=ADVANCED_BREP_SHAPE_REPRESENTATION('',(#219),#2497);
#209=STYLED_ITEM('',(#2708),#219);
#219=MANIFOLD_SOLID_BREP('Body1',#1329);
#229=FACE_BOUND('',#387,.T.);
#230=FACE_BOUND('',#389,.T.);
#280=PLANE('',#1458);
#281=PLANE('',#1459);
#313=FACE_OUTER_BOUND('',#384,.T.);
#314=FACE_OUTER_BOUND('',#385,.T.);
#315=FACE_OUTER_BOUND('',#386,.T.);
#316=FACE_OUTER_BOUND('',#388,.T.);
#384=EDGE_LOOP('',(#932,#933,#934,#935));
#385=EDGE_LOOP('',(#936,#937,#938,#939));
#386=EDGE_LOOP('',(#940));
#387=EDGE_LOOP('',(#941));
#388=EDGE_LOOP('',(#942));
#389=EDGE_LOOP('',(#943));
#506=LINE('',#2091,#562);
#507=LINE('',#2097,#563);
#562=VECTOR('',#1651,0.79);
#563=VECTOR('',#1658,1.065);
#618=CIRCLE('',#1453,0.79);
#619=CIRCLE('',#1454,0.79);
#620=CIRCLE('',#1456,1.065);
#621=CIRCLE('',#1457,1.065);
#690=VERTEX_POINT('',#2088);
#691=VERTEX_POINT('',#2090);
#692=VERTEX_POINT('',#2094);
#693=VERTEX_POINT('',#2096);
#786=EDGE_CURVE('',#690,#690,#618,.T.);
#787=EDGE_CURVE('',#690,#691,#506,.T.);
#788=EDGE_CURVE('',#691,#691,#619,.T.);
#789=EDGE_CURVE('',#692,#692,#620,.T.);
#790=EDGE_CURVE('',#692,#693,#507,.T.);
#791=EDGE_CURVE('',#693,#693,#621,.T.);
#932=ORIENTED_EDGE('',*,*,#786,.F.);
#933=ORIENTED_EDGE('',*,*,#787,.T.);
#934=ORIENTED_EDGE('',*,*,#788,.T.);
#935=ORIENTED_EDGE('',*,*,#787,.F.);
#936=ORIENTED_EDGE('',*,*,#789,.F.);
#937=ORIENTED_EDGE('',*,*,#790,.T.);
#938=ORIENTED_EDGE('',*,*,#791,.T.);
#939=ORIENTED_EDGE('',*,*,#790,.F.);
#940=ORIENTED_EDGE('',*,*,#789,.T.);
#941=ORIENTED_EDGE('',*,*,#786,.T.);
#942=ORIENTED_EDGE('',*,*,#791,.F.);
#943=ORIENTED_EDGE('',*,*,#788,.F.);
#1224=CYLINDRICAL_SURFACE('',#1452,0.79);
#1225=CYLINDRICAL_SURFACE('',#1455,1.065);
#1258=ADVANCED_FACE('',(#313),#1224,.F.);
#1259=ADVANCED_FACE('',(#314),#1225,.T.);
#1260=ADVANCED_FACE('',(#315,#229),#280,.T.);
#1261=ADVANCED_FACE('',(#316,#230),#281,.F.);
#1329=CLOSED_SHELL('',(#1258,#1259,#1260,#1261));
#1451=AXIS2_PLACEMENT_3D('',#2086,#1645,#1646);
#1452=AXIS2_PLACEMENT_3D('',#2087,#1647,#1648);
#1453=AXIS2_PLACEMENT_3D('',#2089,#1649,#1650);
#1454=AXIS2_PLACEMENT_3D('',#2092,#1652,#1653);
#1455=AXIS2_PLACEMENT_3D('',#2093,#1654,#1655);
#1456=AXIS2_PLACEMENT_3D('',#2095,#1656,#1657);
#1457=AXIS2_PLACEMENT_3D('',#2098,#1659,#1660);
#1458=AXIS2_PLACEMENT_3D('',#2099,#1661,#1662);
#1459=AXIS2_PLACEMENT_3D('',#2100,#1663,#1664);
#1645=DIRECTION('axis',(0.,0.,1.));
#1646=DIRECTION('refdir',(1.,0.,0.));
#1647=DIRECTION('center_axis',(1.,0.,0.));
#1648=DIRECTION('ref_axis',(0.,0.,-1.));
#1649=DIRECTION('center_axis',(-1.,0.,0.));
#1650=DIRECTION('ref_axis',(0.,0.,-1.));
#1651=DIRECTION('',(-1.,0.,0.));
#1652=DIRECTION('center_axis',(-1.,0.,0.));
#1653=DIRECTION('ref_axis',(0.,0.,-1.));
#1654=DIRECTION('center_axis',(1.,0.,0.));
#1655=DIRECTION('ref_axis',(0.,0.,-1.));
#1656=DIRECTION('center_axis',(1.,0.,0.));
#1657=DIRECTION('ref_axis',(0.,0.,-1.));
#1658=DIRECTION('',(-1.,0.,0.));
#1659=DIRECTION('center_axis',(1.,0.,0.));
#1660=DIRECTION('ref_axis',(0.,0.,-1.));
#1661=DIRECTION('center_axis',(1.,0.,0.));
#1662=DIRECTION('ref_axis',(0.,0.,-1.));
#1663=DIRECTION('center_axis',(1.,0.,0.));
#1664=DIRECTION('ref_axis',(0.,0.,-1.));
#2086=CARTESIAN_POINT('',(0.,0.,0.));
#2087=CARTESIAN_POINT('Origin',(-10.,0.,0.));
#2088=CARTESIAN_POINT('',(10.,-9.67470971326409E-17,0.79));
#2089=CARTESIAN_POINT('Origin',(10.,0.,0.));
#2090=CARTESIAN_POINT('',(-10.,-9.67470971326409E-17,0.79));
#2091=CARTESIAN_POINT('',(-10.,-9.67470971326409E-17,0.79));
#2092=CARTESIAN_POINT('Origin',(-10.,0.,0.));
#2093=CARTESIAN_POINT('Origin',(-10.,0.,0.));
#2094=CARTESIAN_POINT('',(10.,-1.30424884109193E-16,1.065));
#2095=CARTESIAN_POINT('Origin',(10.,0.,0.));
#2096=CARTESIAN_POINT('',(-10.,-1.30424884109193E-16,1.065));
#2097=CARTESIAN_POINT('',(-10.,-1.30424884109193E-16,1.065));
#2098=CARTESIAN_POINT('Origin',(-10.,0.,0.));
#2099=CARTESIAN_POINT('Origin',(10.,0.,0.));
#2100=CARTESIAN_POINT('Origin',(-10.,0.,0.));
#2485=UNCERTAINTY_MEASURE_WITH_UNIT(LENGTH_MEASURE(0.001),#2508,
'DISTANCE_ACCURACY_VALUE',
'Maximum model space distance between geometric entities at asserted c
onnectivities');
#2495=UNCERTAINTY_MEASURE_WITH_UNIT(LENGTH_MEASURE(0.001),#2508,
'DISTANCE_ACCURACY_VALUE',
'Maximum model space distance between geometric entities at asserted c
onnectivities');
#2497=(
GEOMETRIC_REPRESENTATION_CONTEXT(3)
GLOBAL_UNCERTAINTY_ASSIGNED_CONTEXT((#2485))
GLOBAL_UNIT_ASSIGNED_CONTEXT((#2508,#2510,#2511))
REPRESENTATION_CONTEXT('','3D')
);
#2507=(
GEOMETRIC_REPRESENTATION_CONTEXT(3)
GLOBAL_UNCERTAINTY_ASSIGNED_CONTEXT((#2495))
GLOBAL_UNIT_ASSIGNED_CONTEXT((#2508,#2510,#2511))
REPRESENTATION_CONTEXT('','3D')
);
#2508=(
LENGTH_UNIT()
NAMED_UNIT(*)
SI_UNIT(.CENTI.,.METRE.)
);
#2510=(
NAMED_UNIT(*)
PLANE_ANGLE_UNIT()
SI_UNIT($,.RADIAN.)
);
#2511=(
NAMED_UNIT(*)
SI_UNIT($,.STERADIAN.)
SOLID_ANGLE_UNIT()
);
#2513=SHAPE_DEFINITION_REPRESENTATION(#2524,#2574);
#2524=PRODUCT_DEFINITION_SHAPE('',$,#2586);
#2574=SHAPE_REPRESENTATION('',(#1451),#2497);
#2584=PRODUCT_DEFINITION_CONTEXT('part definition',#2619,'design');
#2586=PRODUCT_DEFINITION('Pipe spool','Pipe spool',#2597,#2584);
#2597=PRODUCT_DEFINITION_FORMATION('',$,#2622);
#2619=APPLICATION_CONTEXT(
'Core Data for Automotive Mechanical Design Process');
#2620=PRODUCT_CONTEXT('part definition',#2619,'mechanical');
#2622=PRODUCT('Pipe spool','Pipe spool','Pipe spool',(#2620));
#2702=COLOUR_RGB('Off White',0.89,0.88,0.83);
#2703=FILL_AREA_STYLE_COLOUR('',#2702);
#2704=FILL_AREA_STYLE('',(#2703));
#2705=SURFACE_STYLE_FILL_AREA(#2704);
#2706=SURFACE_SIDE_STYLE('',(#2705));
#2707=SURFACE_STYLE_USAGE(.BOTH.,#2706);
#2708=PRESENTATION_STYLE_ASSIGNMENT((#2707));
ENDSEC;
END-ISO-10303-21;
